ISO-10303-21;
HEADER;
FILE_DESCRIPTION((''),'2;1');
FILE_NAME('SPRING_ANCHOR_PIN.step','2026-10-01T22:06:14-07:00',(''),(''),'','','');
FILE_SCHEMA (('AUTOMOTIVE_DESIGN { 1 0 10303 214 3 1 1 }'));
ENDSEC;
DATA;
#10=MECHANICAL_DESIGN_GEOMETRIC_PRESENTATION_REPRESENTATION('',(#1035),#50440);
#934=SHAPE_REPRESENTATION_RELATIONSHIP('SRR','None',#50669,#979) ;
#979=ADVANCED_BREP_SHAPE_REPRESENTATION('',(#1088),#50438) ;
#1035=STYLED_ITEM('',(#50883),#1088) ;
#1088=MANIFOLD_SOLID_BREP('SPRING_ANCHOR_PIN',#28713) ;
#1407=FACE_BOUND('',#5712,.T.) ;
#2334=PLANE('',#32268) ;
#2335=PLANE('',#32273) ;
#2336=PLANE('',#32276) ;
#3862=FACE_OUTER_BOUND('',#5711,.T.) ;
#3863=FACE_OUTER_BOUND('',#5713,.T.) ;
#3864=FACE_OUTER_BOUND('',#5714,.T.) ;
#3865=FACE_OUTER_BOUND('',#5715,.T.) ;
#3866=FACE_OUTER_BOUND('',#5716,.T.) ;
#5711=EDGE_LOOP('',(#26487)) ;
#5712=EDGE_LOOP('',(#26488)) ;
#5713=EDGE_LOOP('',(#26489,#26490,#26491,#26492)) ;
#5714=EDGE_LOOP('',(#26493)) ;
#5715=EDGE_LOOP('',(#26494,#26495,#26496,#26497)) ;
#5716=EDGE_LOOP('',(#26498)) ;
#8201=LINE('',#50106,#10673) ;
#8202=LINE('',#50110,#10674) ;
#10673=VECTOR('',#40972,0.45) ;
#10674=VECTOR('',#40977,0.245) ;
#11814=CIRCLE('',#32269,0.45) ;
#11815=CIRCLE('',#32270,0.245) ;
#11816=CIRCLE('',#32272,0.45) ;
#11817=CIRCLE('',#32275,0.245) ;
#14508=VERTEX_POINT('',#50099) ;
#14509=VERTEX_POINT('',#50101) ;
#14510=VERTEX_POINT('',#50104) ;
#14511=VERTEX_POINT('',#50109) ;
#18509=EDGE_CURVE('',#14508,#14508,#11814,.T.) ;
#18510=EDGE_CURVE('',#14509,#14509,#11815,.T.) ;
#18511=EDGE_CURVE('',#14510,#14510,#11816,.T.) ;
#18512=EDGE_CURVE('',#14510,#14508,#8201,.T.) ;
#18513=EDGE_CURVE('',#14509,#14511,#8202,.T.) ;
#18514=EDGE_CURVE('',#14511,#14511,#11817,.T.) ;
#26487=ORIENTED_EDGE('',*,*,#18509,.T.) ;
#26488=ORIENTED_EDGE('',*,*,#18510,.T.) ;
#26489=ORIENTED_EDGE('',*,*,#18511,.F.) ;
#26490=ORIENTED_EDGE('',*,*,#18512,.T.) ;
#26491=ORIENTED_EDGE('',*,*,#18509,.F.) ;
#26492=ORIENTED_EDGE('',*,*,#18512,.F.) ;
#26493=ORIENTED_EDGE('',*,*,#18511,.T.) ;
#26494=ORIENTED_EDGE('',*,*,#18510,.F.) ;
#26495=ORIENTED_EDGE('',*,*,#18513,.T.) ;
#26496=ORIENTED_EDGE('',*,*,#18514,.F.) ;
#26497=ORIENTED_EDGE('',*,*,#18513,.F.) ;
#26498=ORIENTED_EDGE('',*,*,#18514,.T.) ;
#27060=CYLINDRICAL_SURFACE('',#32271,0.45) ;
#27061=CYLINDRICAL_SURFACE('',#32274,0.245) ;
#28597=ADVANCED_FACE('',(#3862,#1407),#2334,.T.) ;
#28598=ADVANCED_FACE('',(#3863),#27060,.T.) ;
#28599=ADVANCED_FACE('',(#3864),#2335,.T.) ;
#28600=ADVANCED_FACE('',(#3865),#27061,.T.) ;
#28601=ADVANCED_FACE('',(#3866),#2336,.T.) ;
#28713=CLOSED_SHELL('',(#28597,#28598,#28599,#28600,#28601)) ;
#32267=AXIS2_PLACEMENT_3D('',#50097,#40960,#40961) ;
#32268=AXIS2_PLACEMENT_3D('',#50098,#40962,#40963) ;
#32269=AXIS2_PLACEMENT_3D('',#50100,#40964,#40965) ;
#32270=AXIS2_PLACEMENT_3D('',#50102,#40966,#40967) ;
#32271=AXIS2_PLACEMENT_3D('',#50103,#40968,#40969) ;
#32272=AXIS2_PLACEMENT_3D('',#50105,#40970,#40971) ;
#32273=AXIS2_PLACEMENT_3D('',#50107,#40973,#40974) ;
#32274=AXIS2_PLACEMENT_3D('',#50108,#40975,#40976) ;
#32275=AXIS2_PLACEMENT_3D('',#50111,#40978,#40979) ;
#32276=AXIS2_PLACEMENT_3D('',#50112,#40980,#40981) ;
#40960=DIRECTION('axis',(0.,0.,1.)) ;
#40961=DIRECTION('refdir',(1.,0.,0.)) ;
#40962=DIRECTION('center_axis',(0.,0.,-1.)) ;
#40963=DIRECTION('ref_axis',(-1.,0.,0.)) ;
#40964=DIRECTION('center_axis',(0.,0.,-1.)) ;
#40965=DIRECTION('ref_axis',(1.,0.,0.)) ;
#40966=DIRECTION('center_axis',(0.,0.,1.)) ;
#40967=DIRECTION('ref_axis',(1.,0.,0.)) ;
#40968=DIRECTION('center_axis',(0.,0.,1.)) ;
#40969=DIRECTION('ref_axis',(1.,0.,0.)) ;
#40970=DIRECTION('center_axis',(0.,0.,1.)) ;
#40971=DIRECTION('ref_axis',(1.,0.,0.)) ;
#40972=DIRECTION('',(0.,0.,-1.)) ;
#40973=DIRECTION('center_axis',(0.,0.,1.)) ;
#40974=DIRECTION('ref_axis',(1.,0.,0.)) ;
#40975=DIRECTION('center_axis',(0.,0.,1.)) ;
#40976=DIRECTION('ref_axis',(1.,0.,0.)) ;
#40977=DIRECTION('',(0.,0.,-1.)) ;
#40978=DIRECTION('center_axis',(0.,0.,-1.)) ;
#40979=DIRECTION('ref_axis',(1.,0.,0.)) ;
#40980=DIRECTION('center_axis',(0.,0.,-1.)) ;
#40981=DIRECTION('ref_axis',(-1.,0.,0.)) ;
#50097=CARTESIAN_POINT('',(0.,0.,0.)) ;
#50098=CARTESIAN_POINT('Origin',(0.,0.,44.8)) ;
#50099=CARTESIAN_POINT('',(-0.45,-5.51091059616309E-17,44.8)) ;
#50100=CARTESIAN_POINT('Origin',(0.,0.,44.8)) ;
#50101=CARTESIAN_POINT('',(-0.245,-3.00038465791102E-17,44.8)) ;
#50102=CARTESIAN_POINT('Origin',(0.,0.,44.8)) ;
#50103=CARTESIAN_POINT('Origin',(0.,0.,44.9)) ;
#50104=CARTESIAN_POINT('',(-0.45,-5.51091059616309E-17,45.)) ;
#50105=CARTESIAN_POINT('Origin',(0.,0.,45.)) ;
#50106=CARTESIAN_POINT('',(-0.45,-5.51091059616309E-17,44.9)) ;
#50107=CARTESIAN_POINT('Origin',(0.,0.,45.)) ;
#50108=CARTESIAN_POINT('Origin',(0.,0.,43.7)) ;
#50109=CARTESIAN_POINT('',(-0.245,-3.00038465791102E-17,42.6)) ;
#50110=CARTESIAN_POINT('',(-0.245,-3.00038465791102E-17,43.7)) ;
#50111=CARTESIAN_POINT('Origin',(0.,0.,42.6)) ;
#50112=CARTESIAN_POINT('Origin',(0.,0.,42.6)) ;
#50385=UNCERTAINTY_MEASURE_WITH_UNIT(LENGTH_MEASURE(0.001),#50441,
'DISTANCE_ACCURACY_VALUE',
'Maximum model space distance between geometric entities at asserted c
onnectivities') ;
#50387=UNCERTAINTY_MEASURE_WITH_UNIT(LENGTH_MEASURE(0.001),#50441,
'DISTANCE_ACCURACY_VALUE',
'Maximum model space distance between geometric entities at asserted c
onnectivities') ;
#50438=(
GEOMETRIC_REPRESENTATION_CONTEXT(3)
GLOBAL_UNCERTAINTY_ASSIGNED_CONTEXT((#50385))
GLOBAL_UNIT_ASSIGNED_CONTEXT((#50441,#50443,#50444))
REPRESENTATION_CONTEXT('','3D')
) ;
#50440=(
GEOMETRIC_REPRESENTATION_CONTEXT(3)
GLOBAL_UNCERTAINTY_ASSIGNED_CONTEXT((#50387))
GLOBAL_UNIT_ASSIGNED_CONTEXT((#50441,#50443,#50444))
REPRESENTATION_CONTEXT('','3D')
) ;
#50441=(
LENGTH_UNIT()
NAMED_UNIT(*)
SI_UNIT(.CENTI.,.METRE.)
) ;
#50443=(
NAMED_UNIT(*)
PLANE_ANGLE_UNIT()
SI_UNIT($,.RADIAN.)
) ;
#50444=(
NAMED_UNIT(*)
SI_UNIT($,.STERADIAN.)
SOLID_ANGLE_UNIT()
) ;
#50495=SHAPE_DEFINITION_REPRESENTATION(#50591,#50669) ;
#50591=PRODUCT_DEFINITION_SHAPE('',$,#50722) ;
#50669=SHAPE_REPRESENTATION('',(#32267),#50438) ;
#50671=PRODUCT_DEFINITION_CONTEXT('part definition',#50829,'design') ;
#50722=PRODUCT_DEFINITION('SPRING_ANCHOR_PIN','SPRING_ANCHOR_PIN',
#50774,#50671) ;
#50774=PRODUCT_DEFINITION_FORMATION('',$,#50881) ;
#50829=APPLICATION_CONTEXT(
'Core Data for Automotive Mechanical Design Process') ;
#50830=PRODUCT_CONTEXT('part definition',#50829,'mechanical') ;
#50881=PRODUCT('SPRING_ANCHOR_PIN','SPRING_ANCHOR_PIN',$,(#50830)) ;
#50883=PRESENTATION_STYLE_ASSIGNMENT((#50890)) ;
#50890=SURFACE_STYLE_USAGE(.BOTH.,#50897) ;
#50897=SURFACE_SIDE_STYLE('',(#50904)) ;
#50904=SURFACE_STYLE_FILL_AREA(#50911) ;
#50911=FILL_AREA_STYLE('Steel - Satin',(#50918)) ;
#50918=FILL_AREA_STYLE_COLOUR('Steel - Satin',#50925) ;
#50925=COLOUR_RGB('Steel - Satin', 0.31764706, 0.68627451, 0.89019608) ;
ENDSEC;
END-ISO-10303-21;
